ISO-10303-21;
HEADER;
/* Generated by software containing ST-Developer
 * from STEP Tools, Inc. (www.steptools.com) 
 */

FILE_DESCRIPTION(
/* description */ ('Quick-return (Whitworth) mechanism'),
/* implementation_level */ '2;1');

FILE_NAME(
/* name */ 'M4x10 Cap Screw.step',
/* time_stamp */ '2026-10-28T03:25:57-07:00',
/* author */ (''),
/* organization */ (''),
/* preprocessor_version */ 'ST-DEVELOPER v20.2',
/* originating_system */ 'Autodesk Translation Framework v15.17.0.0',
/* authorisation */ '');

FILE_SCHEMA (('AUTOMOTIVE_DESIGN { 1 0 10303 214 3 1 1 }'));
ENDSEC;

DATA;
#10=MECHANICAL_DESIGN_GEOMETRIC_PRESENTATION_REPRESENTATION('',(#541),#14878);
#13=ORIENTED_CLOSED_SHELL('',*,#7897,.F.);
#16=BREP_WITH_VOIDS('Body1',#7898,(#13));
#361=CONICAL_SURFACE('',#9319,0.325,0.785398163397448);
#362=CONICAL_SURFACE('',#9323,0.335,0.785398163397448);
#363=CONICAL_SURFACE('',#9327,0.21,0.463647609000806);
#445=SHAPE_REPRESENTATION_RELATIONSHIP('SRR','None',#15120,#489);
#489=ADVANCED_BREP_SHAPE_REPRESENTATION('',(#16),#14877);
#541=STYLED_ITEM('',(#15413),#16);
#781=FACE_BOUND('',#2167,.T.);
#1036=PLANE('',#9307);
#1037=PLANE('',#9308);
#1038=PLANE('',#9309);
#1039=PLANE('',#9310);
#1040=PLANE('',#9311);
#1041=PLANE('',#9312);
#1042=PLANE('',#9313);
#1043=PLANE('',#9314);
#1044=PLANE('',#9315);
#1045=PLANE('',#9317);
#1046=PLANE('',#9325);
#1497=FACE_OUTER_BOUND('',#2153,.T.);
#1498=FACE_OUTER_BOUND('',#2154,.T.);
#1499=FACE_OUTER_BOUND('',#2155,.T.);
#1500=FACE_OUTER_BOUND('',#2156,.T.);
#1501=FACE_OUTER_BOUND('',#2157,.T.);
#1502=FACE_OUTER_BOUND('',#2158,.T.);
#1503=FACE_OUTER_BOUND('',#2159,.T.);
#1504=FACE_OUTER_BOUND('',#2160,.T.);
#1505=FACE_OUTER_BOUND('',#2161,.T.);
#1506=FACE_OUTER_BOUND('',#2162,.T.);
#1507=FACE_OUTER_BOUND('',#2163,.T.);
#1508=FACE_OUTER_BOUND('',#2164,.T.);
#1509=FACE_OUTER_BOUND('',#2165,.T.);
#1510=FACE_OUTER_BOUND('',#2166,.T.);
#1511=FACE_OUTER_BOUND('',#2168,.T.);
#1512=FACE_OUTER_BOUND('',#2169,.T.);
#2153=EDGE_LOOP('',(#7150,#7151,#7152,#7153));
#2154=EDGE_LOOP('',(#7154,#7155,#7156,#7157));
#2155=EDGE_LOOP('',(#7158,#7159,#7160,#7161));
#2156=EDGE_LOOP('',(#7162,#7163,#7164,#7165));
#2157=EDGE_LOOP('',(#7166,#7167,#7168,#7169));
#2158=EDGE_LOOP('',(#7170,#7171,#7172,#7173));
#2159=EDGE_LOOP('',(#7174,#7175,#7176,#7177,#7178,#7179));
#2160=EDGE_LOOP('',(#7180,#7181,#7182,#7183,#7184,#7185));
#2161=EDGE_LOOP('',(#7186));
#2162=EDGE_LOOP('',(#7187));
#2163=EDGE_LOOP('',(#7188,#7189,#7190,#7191));
#2164=EDGE_LOOP('',(#7192,#7193,#7194,#7195));
#2165=EDGE_LOOP('',(#7196,#7197,#7198,#7199));
#2166=EDGE_LOOP('',(#7200));
#2167=EDGE_LOOP('',(#7201));
#2168=EDGE_LOOP('',(#7202,#7203,#7204,#7205));
#2169=EDGE_LOOP('',(#7206,#7207,#7208,#7209));
#2670=LINE('',#14642,#3193);
#2671=LINE('',#14644,#3194);
#2672=LINE('',#14646,#3195);
#2673=LINE('',#14647,#3196);
#2674=LINE('',#14650,#3197);
#2675=LINE('',#14652,#3198);
#2676=LINE('',#14653,#3199);
#2677=LINE('',#14656,#3200);
#2678=LINE('',#14658,#3201);
#2679=LINE('',#14659,#3202);
#2680=LINE('',#14662,#3203);
#2681=LINE('',#14664,#3204);
#2682=LINE('',#14665,#3205);
#2683=LINE('',#14668,#3206);
#2684=LINE('',#14670,#3207);
#2685=LINE('',#14671,#3208);
#2686=LINE('',#14673,#3209);
#2687=LINE('',#14674,#3210);
#2688=LINE('',#14686,#3211);
#2689=LINE('',#14690,#3212);
#2690=LINE('',#14694,#3213);
#2691=LINE('',#14701,#3214);
#2692=LINE('',#14703,#3215);
#3193=VECTOR('',#11745,1.);
#3194=VECTOR('',#11746,1.);
#3195=VECTOR('',#11747,1.);
#3196=VECTOR('',#11748,1.);
#3197=VECTOR('',#11751,1.);
#3198=VECTOR('',#11752,1.);
#3199=VECTOR('',#11753,1.);
#3200=VECTOR('',#11756,1.);
#3201=VECTOR('',#11757,1.);
#3202=VECTOR('',#11758,1.);
#3203=VECTOR('',#11761,1.);
#3204=VECTOR('',#11762,1.);
#3205=VECTOR('',#11763,1.);
#3206=VECTOR('',#11766,1.);
#3207=VECTOR('',#11767,1.);
#3208=VECTOR('',#11768,1.);
#3209=VECTOR('',#11771,1.);
#3210=VECTOR('',#11772,1.);
#3211=VECTOR('',#11789,0.325);
#3212=VECTOR('',#11794,0.35);
#3213=VECTOR('',#11799,0.335);
#3214=VECTOR('',#11808,0.21);
#3215=VECTOR('',#11811,0.2);
#3624=CIRCLE('',#9316,0.1954);
#3625=CIRCLE('',#9318,0.3);
#3626=CIRCLE('',#9320,0.35);
#3627=CIRCLE('',#9322,0.35);
#3628=CIRCLE('',#9324,0.32);
#3629=CIRCLE('',#9326,0.22);
#3630=CIRCLE('',#9328,0.1954);
#4269=VERTEX_POINT('',#14640);
#4270=VERTEX_POINT('',#14641);
#4271=VERTEX_POINT('',#14643);
#4272=VERTEX_POINT('',#14645);
#4273=VERTEX_POINT('',#14649);
#4274=VERTEX_POINT('',#14651);
#4275=VERTEX_POINT('',#14655);
#4276=VERTEX_POINT('',#14657);
#4277=VERTEX_POINT('',#14661);
#4278=VERTEX_POINT('',#14663);
#4279=VERTEX_POINT('',#14667);
#4280=VERTEX_POINT('',#14669);
#4281=VERTEX_POINT('',#14678);
#4282=VERTEX_POINT('',#14681);
#4283=VERTEX_POINT('',#14684);
#4284=VERTEX_POINT('',#14688);
#4285=VERTEX_POINT('',#14692);
#4286=VERTEX_POINT('',#14696);
#4287=VERTEX_POINT('',#14699);
#5232=EDGE_CURVE('',#4269,#4270,#2670,.T.);
#5233=EDGE_CURVE('',#4270,#4271,#2671,.T.);
#5234=EDGE_CURVE('',#4271,#4272,#2672,.T.);
#5235=EDGE_CURVE('',#4269,#4272,#2673,.T.);
#5236=EDGE_CURVE('',#4270,#4273,#2674,.T.);
#5237=EDGE_CURVE('',#4273,#4274,#2675,.T.);
#5238=EDGE_CURVE('',#4274,#4271,#2676,.T.);
#5239=EDGE_CURVE('',#4273,#4275,#2677,.T.);
#5240=EDGE_CURVE('',#4275,#4276,#2678,.T.);
#5241=EDGE_CURVE('',#4276,#4274,#2679,.T.);
#5242=EDGE_CURVE('',#4275,#4277,#2680,.T.);
#5243=EDGE_CURVE('',#4277,#4278,#2681,.T.);
#5244=EDGE_CURVE('',#4278,#4276,#2682,.T.);
#5245=EDGE_CURVE('',#4277,#4279,#2683,.T.);
#5246=EDGE_CURVE('',#4279,#4280,#2684,.T.);
#5247=EDGE_CURVE('',#4280,#4278,#2685,.T.);
#5248=EDGE_CURVE('',#4279,#4269,#2686,.T.);
#5249=EDGE_CURVE('',#4272,#4280,#2687,.T.);
#5250=EDGE_CURVE('',#4281,#4281,#3624,.T.);
#5251=EDGE_CURVE('',#4282,#4282,#3625,.T.);
#5252=EDGE_CURVE('',#4283,#4283,#3626,.T.);
#5253=EDGE_CURVE('',#4283,#4282,#2688,.T.);
#5254=EDGE_CURVE('',#4284,#4284,#3627,.T.);
#5255=EDGE_CURVE('',#4284,#4283,#2689,.T.);
#5256=EDGE_CURVE('',#4285,#4285,#3628,.T.);
#5257=EDGE_CURVE('',#4285,#4284,#2690,.T.);
#5258=EDGE_CURVE('',#4286,#4286,#3629,.T.);
#5259=EDGE_CURVE('',#4287,#4287,#3630,.F.);
#5260=EDGE_CURVE('',#4287,#4286,#2691,.T.);
#5261=EDGE_CURVE('',#4281,#4287,#2692,.T.);
#7150=ORIENTED_EDGE('',*,*,#5232,.T.);
#7151=ORIENTED_EDGE('',*,*,#5233,.T.);
#7152=ORIENTED_EDGE('',*,*,#5234,.T.);
#7153=ORIENTED_EDGE('',*,*,#5235,.F.);
#7154=ORIENTED_EDGE('',*,*,#5236,.T.);
#7155=ORIENTED_EDGE('',*,*,#5237,.T.);
#7156=ORIENTED_EDGE('',*,*,#5238,.T.);
#7157=ORIENTED_EDGE('',*,*,#5233,.F.);
#7158=ORIENTED_EDGE('',*,*,#5239,.T.);
#7159=ORIENTED_EDGE('',*,*,#5240,.T.);
#7160=ORIENTED_EDGE('',*,*,#5241,.T.);
#7161=ORIENTED_EDGE('',*,*,#5237,.F.);
#7162=ORIENTED_EDGE('',*,*,#5242,.T.);
#7163=ORIENTED_EDGE('',*,*,#5243,.T.);
#7164=ORIENTED_EDGE('',*,*,#5244,.T.);
#7165=ORIENTED_EDGE('',*,*,#5240,.F.);
#7166=ORIENTED_EDGE('',*,*,#5245,.T.);
#7167=ORIENTED_EDGE('',*,*,#5246,.T.);
#7168=ORIENTED_EDGE('',*,*,#5247,.T.);
#7169=ORIENTED_EDGE('',*,*,#5243,.F.);
#7170=ORIENTED_EDGE('',*,*,#5248,.T.);
#7171=ORIENTED_EDGE('',*,*,#5235,.T.);
#7172=ORIENTED_EDGE('',*,*,#5249,.T.);
#7173=ORIENTED_EDGE('',*,*,#5246,.F.);
#7174=ORIENTED_EDGE('',*,*,#5248,.F.);
#7175=ORIENTED_EDGE('',*,*,#5245,.F.);
#7176=ORIENTED_EDGE('',*,*,#5242,.F.);
#7177=ORIENTED_EDGE('',*,*,#5239,.F.);
#7178=ORIENTED_EDGE('',*,*,#5236,.F.);
#7179=ORIENTED_EDGE('',*,*,#5232,.F.);
#7180=ORIENTED_EDGE('',*,*,#5249,.F.);
#7181=ORIENTED_EDGE('',*,*,#5234,.F.);
#7182=ORIENTED_EDGE('',*,*,#5238,.F.);
#7183=ORIENTED_EDGE('',*,*,#5241,.F.);
#7184=ORIENTED_EDGE('',*,*,#5244,.F.);
#7185=ORIENTED_EDGE('',*,*,#5247,.F.);
#7186=ORIENTED_EDGE('',*,*,#5250,.F.);
#7187=ORIENTED_EDGE('',*,*,#5251,.F.);
#7188=ORIENTED_EDGE('',*,*,#5252,.F.);
#7189=ORIENTED_EDGE('',*,*,#5253,.T.);
#7190=ORIENTED_EDGE('',*,*,#5251,.T.);
#7191=ORIENTED_EDGE('',*,*,#5253,.F.);
#7192=ORIENTED_EDGE('',*,*,#5254,.F.);
#7193=ORIENTED_EDGE('',*,*,#5255,.T.);
#7194=ORIENTED_EDGE('',*,*,#5252,.T.);
#7195=ORIENTED_EDGE('',*,*,#5255,.F.);
#7196=ORIENTED_EDGE('',*,*,#5256,.F.);
#7197=ORIENTED_EDGE('',*,*,#5257,.T.);
#7198=ORIENTED_EDGE('',*,*,#5254,.T.);
#7199=ORIENTED_EDGE('',*,*,#5257,.F.);
#7200=ORIENTED_EDGE('',*,*,#5256,.T.);
#7201=ORIENTED_EDGE('',*,*,#5258,.F.);
#7202=ORIENTED_EDGE('',*,*,#5259,.F.);
#7203=ORIENTED_EDGE('',*,*,#5260,.T.);
#7204=ORIENTED_EDGE('',*,*,#5258,.T.);
#7205=ORIENTED_EDGE('',*,*,#5260,.F.);
#7206=ORIENTED_EDGE('',*,*,#5250,.T.);
#7207=ORIENTED_EDGE('',*,*,#5261,.T.);
#7208=ORIENTED_EDGE('',*,*,#5259,.T.);
#7209=ORIENTED_EDGE('',*,*,#5261,.F.);
#7376=CYLINDRICAL_SURFACE('',#9321,0.35);
#7377=CYLINDRICAL_SURFACE('',#9329,0.1954);
#7828=ADVANCED_FACE('',(#1497),#1036,.F.);
#7829=ADVANCED_FACE('',(#1498),#1037,.F.);
#7830=ADVANCED_FACE('',(#1499),#1038,.F.);
#7831=ADVANCED_FACE('',(#1500),#1039,.F.);
#7832=ADVANCED_FACE('',(#1501),#1040,.F.);
#7833=ADVANCED_FACE('',(#1502),#1041,.F.);
#7834=ADVANCED_FACE('',(#1503),#1042,.F.);
#7835=ADVANCED_FACE('',(#1504),#1043,.F.);
#7836=ADVANCED_FACE('',(#1505),#1044,.F.);
#7837=ADVANCED_FACE('',(#1506),#1045,.T.);
#7838=ADVANCED_FACE('',(#1507),#361,.T.);
#7839=ADVANCED_FACE('',(#1508),#7376,.T.);
#7840=ADVANCED_FACE('',(#1509),#362,.T.);
#7841=ADVANCED_FACE('',(#1510,#781),#1046,.T.);
#7842=ADVANCED_FACE('',(#1511),#363,.T.);
#7843=ADVANCED_FACE('',(#1512),#7377,.T.);
#7897=CLOSED_SHELL('',(#7828,#7829,#7830,#7831,#7832,#7833,#7834,#7835));
#7898=CLOSED_SHELL('',(#7836,#7837,#7838,#7839,#7840,#7841,#7842,#7843));
#9306=AXIS2_PLACEMENT_3D('',#14638,#11741,#11742);
#9307=AXIS2_PLACEMENT_3D('',#14639,#11743,#11744);
#9308=AXIS2_PLACEMENT_3D('',#14648,#11749,#11750);
#9309=AXIS2_PLACEMENT_3D('',#14654,#11754,#11755);
#9310=AXIS2_PLACEMENT_3D('',#14660,#11759,#11760);
#9311=AXIS2_PLACEMENT_3D('',#14666,#11764,#11765);
#9312=AXIS2_PLACEMENT_3D('',#14672,#11769,#11770);
#9313=AXIS2_PLACEMENT_3D('',#14675,#11773,#11774);
#9314=AXIS2_PLACEMENT_3D('',#14676,#11775,#11776);
#9315=AXIS2_PLACEMENT_3D('',#14677,#11777,#11778);
#9316=AXIS2_PLACEMENT_3D('',#14679,#11779,#11780);
#9317=AXIS2_PLACEMENT_3D('',#14680,#11781,#11782);
#9318=AXIS2_PLACEMENT_3D('',#14682,#11783,#11784);
#9319=AXIS2_PLACEMENT_3D('',#14683,#11785,#11786);
#9320=AXIS2_PLACEMENT_3D('',#14685,#11787,#11788);
#9321=AXIS2_PLACEMENT_3D('',#14687,#11790,#11791);
#9322=AXIS2_PLACEMENT_3D('',#14689,#11792,#11793);
#9323=AXIS2_PLACEMENT_3D('',#14691,#11795,#11796);
#9324=AXIS2_PLACEMENT_3D('',#14693,#11797,#11798);
#9325=AXIS2_PLACEMENT_3D('',#14695,#11800,#11801);
#9326=AXIS2_PLACEMENT_3D('',#14697,#11802,#11803);
#9327=AXIS2_PLACEMENT_3D('',#14698,#11804,#11805);
#9328=AXIS2_PLACEMENT_3D('',#14700,#11806,#11807);
#9329=AXIS2_PLACEMENT_3D('',#14702,#11809,#11810);
#11741=DIRECTION('axis',(0.,0.,1.));
#11742=DIRECTION('refdir',(1.,0.,0.));
#11743=DIRECTION('center_axis',(0.866025403784439,0.,-0.5));
#11744=DIRECTION('ref_axis',(0.5,0.,0.866025403784439));
#11745=DIRECTION('',(-0.5,0.,-0.866025403784439));
#11746=DIRECTION('',(0.,-1.,0.));
#11747=DIRECTION('',(0.5,0.,0.866025403784439));
#11748=DIRECTION('',(0.,-1.,0.));
#11749=DIRECTION('center_axis',(1.60246890531964E-16,0.,-1.));
#11750=DIRECTION('ref_axis',(1.,0.,1.60246890531964E-16));
#11751=DIRECTION('',(-1.,0.,-1.60246890531964E-16));
#11752=DIRECTION('',(0.,-1.,0.));
#11753=DIRECTION('',(1.,0.,1.60246890531964E-16));
#11754=DIRECTION('center_axis',(-0.866025403784439,0.,-0.5));
#11755=DIRECTION('ref_axis',(0.5,0.,-0.866025403784439));
#11756=DIRECTION('',(-0.5,0.,0.866025403784439));
#11757=DIRECTION('',(0.,-1.,0.));
#11758=DIRECTION('',(0.5,0.,-0.866025403784439));
#11759=DIRECTION('center_axis',(-0.866025403784439,0.,0.5));
#11760=DIRECTION('ref_axis',(-0.5,0.,-0.866025403784439));
#11761=DIRECTION('',(0.5,0.,0.866025403784439));
#11762=DIRECTION('',(0.,-1.,0.));
#11763=DIRECTION('',(-0.5,0.,-0.866025403784439));
#11764=DIRECTION('center_axis',(-1.60246890531964E-16,0.,1.));
#11765=DIRECTION('ref_axis',(-1.,0.,-1.60246890531964E-16));
#11766=DIRECTION('',(1.,0.,1.60246890531964E-16));
#11767=DIRECTION('',(0.,-1.,0.));
#11768=DIRECTION('',(-1.,0.,-1.60246890531964E-16));
#11769=DIRECTION('center_axis',(0.866025403784439,0.,0.5));
#11770=DIRECTION('ref_axis',(-0.5,0.,0.866025403784439));
#11771=DIRECTION('',(0.5,0.,-0.866025403784439));
#11772=DIRECTION('',(-0.5,0.,0.866025403784439));
#11773=DIRECTION('center_axis',(0.,1.,0.));
#11774=DIRECTION('ref_axis',(1.,0.,0.));
#11775=DIRECTION('center_axis',(0.,-1.,0.));
#11776=DIRECTION('ref_axis',(0.,0.,-1.));
#11777=DIRECTION('center_axis',(0.,1.,0.));
#11778=DIRECTION('ref_axis',(1.,0.,0.));
#11779=DIRECTION('center_axis',(0.,1.,0.));
#11780=DIRECTION('ref_axis',(1.,0.,0.));
#11781=DIRECTION('center_axis',(0.,1.,0.));
#11782=DIRECTION('ref_axis',(0.,0.,1.));
#11783=DIRECTION('center_axis',(0.,-1.,0.));
#11784=DIRECTION('ref_axis',(1.,0.,0.));
#11785=DIRECTION('center_axis',(0.,-1.,0.));
#11786=DIRECTION('ref_axis',(1.,0.,0.));
#11787=DIRECTION('center_axis',(0.,-1.,0.));
#11788=DIRECTION('ref_axis',(1.,0.,0.));
#11789=DIRECTION('',(0.707106781186547,0.707106781186548,8.65956056235493E-17));
#11790=DIRECTION('center_axis',(0.,-1.,0.));
#11791=DIRECTION('ref_axis',(1.,0.,0.));
#11792=DIRECTION('center_axis',(0.,-1.,0.));
#11793=DIRECTION('ref_axis',(1.,0.,0.));
#11794=DIRECTION('',(0.,1.,0.));
#11795=DIRECTION('center_axis',(0.,1.,0.));
#11796=DIRECTION('ref_axis',(1.,0.,0.));
#11797=DIRECTION('center_axis',(0.,-1.,0.));
#11798=DIRECTION('ref_axis',(1.,0.,0.));
#11799=DIRECTION('',(-0.707106781186547,0.707106781186548,-8.65956056235493E-17));
#11800=DIRECTION('center_axis',(0.,-1.,0.));
#11801=DIRECTION('ref_axis',(0.,0.,-1.));
#11802=DIRECTION('center_axis',(0.,-1.,0.));
#11803=DIRECTION('ref_axis',(1.,0.,0.));
#11804=DIRECTION('center_axis',(0.,1.,0.));
#11805=DIRECTION('ref_axis',(1.,0.,0.));
#11806=DIRECTION('center_axis',(0.,1.,0.));
#11807=DIRECTION('ref_axis',(1.,0.,0.));
#11808=DIRECTION('',(-0.447213595499958,0.894427190999916,-5.47678698264203E-17));
#11809=DIRECTION('center_axis',(0.,-1.,0.));
#11810=DIRECTION('ref_axis',(1.,0.,0.));
#11811=DIRECTION('',(0.,1.,0.));
#14638=CARTESIAN_POINT('',(0.,0.,0.));
#14639=CARTESIAN_POINT('Origin',(0.0866025403784439,-0.4,-0.15));
#14640=CARTESIAN_POINT('',(0.173205080756888,-0.4,0.));
#14641=CARTESIAN_POINT('',(0.0866025403784439,-0.4,-0.15));
#14642=CARTESIAN_POINT('',(0.173205080756888,-0.4,0.));
#14643=CARTESIAN_POINT('',(0.0866025403784439,-0.64,-0.15));
#14644=CARTESIAN_POINT('',(0.0866025403784439,-0.4,-0.15));
#14645=CARTESIAN_POINT('',(0.173205080756888,-0.64,0.));
#14646=CARTESIAN_POINT('',(0.173205080756888,-0.64,0.));
#14647=CARTESIAN_POINT('',(0.173205080756888,-0.4,0.));
#14648=CARTESIAN_POINT('Origin',(-0.0866025403784438,-0.4,-0.15));
#14649=CARTESIAN_POINT('',(-0.0866025403784438,-0.4,-0.15));
#14650=CARTESIAN_POINT('',(0.0866025403784439,-0.4,-0.15));
#14651=CARTESIAN_POINT('',(-0.0866025403784438,-0.64,-0.15));
#14652=CARTESIAN_POINT('',(-0.0866025403784438,-0.4,-0.15));
#14653=CARTESIAN_POINT('',(0.0866025403784439,-0.64,-0.15));
#14654=CARTESIAN_POINT('Origin',(-0.173205080756888,-0.4,-2.77555756156289E-17));
#14655=CARTESIAN_POINT('',(-0.173205080756888,-0.4,-2.12115047744981E-17));
#14656=CARTESIAN_POINT('',(-0.0866025403784438,-0.4,-0.15));
#14657=CARTESIAN_POINT('',(-0.173205080756888,-0.64,-2.77555756156289E-17));
#14658=CARTESIAN_POINT('',(-0.173205080756888,-0.4,-2.12115047744981E-17));
#14659=CARTESIAN_POINT('',(-0.0866025403784438,-0.64,-0.15));
#14660=CARTESIAN_POINT('Origin',(-0.0866025403784439,-0.4,0.15));
#14661=CARTESIAN_POINT('',(-0.0866025403784439,-0.4,0.15));
#14662=CARTESIAN_POINT('',(-0.173205080756888,-0.4,-2.12115047744981E-17));
#14663=CARTESIAN_POINT('',(-0.0866025403784439,-0.64,0.15));
#14664=CARTESIAN_POINT('',(-0.0866025403784439,-0.4,0.15));
#14665=CARTESIAN_POINT('',(-0.173205080756888,-0.64,-2.12115047744981E-17));
#14666=CARTESIAN_POINT('Origin',(0.0866025403784439,-0.4,0.15));
#14667=CARTESIAN_POINT('',(0.0866025403784439,-0.4,0.15));
#14668=CARTESIAN_POINT('',(-0.0866025403784439,-0.4,0.15));
#14669=CARTESIAN_POINT('',(0.0866025403784439,-0.64,0.15));
#14670=CARTESIAN_POINT('',(0.0866025403784439,-0.4,0.15));
#14671=CARTESIAN_POINT('',(-0.0866025403784439,-0.64,0.15));
#14672=CARTESIAN_POINT('Origin',(0.173205080756888,-0.4,0.));
#14673=CARTESIAN_POINT('',(0.0866025403784439,-0.4,0.15));
#14674=CARTESIAN_POINT('',(0.0866025403784439,-0.64,0.15));
#14675=CARTESIAN_POINT('Origin',(0.,-0.4,-2.77555756156289E-17));
#14676=CARTESIAN_POINT('Origin',(0.,-0.64,-2.77555756156289E-17));
#14677=CARTESIAN_POINT('Origin',(0.,-1.,0.));
#14678=CARTESIAN_POINT('',(-0.1954,-1.,2.39295984553393E-17));
#14679=CARTESIAN_POINT('Origin',(0.,-1.,0.));
#14680=CARTESIAN_POINT('Origin',(0.3,0.4,0.));
#14681=CARTESIAN_POINT('',(-0.3,0.4,-3.67394039744206E-17));
#14682=CARTESIAN_POINT('Origin',(0.,0.4,0.));
#14683=CARTESIAN_POINT('Origin',(0.,0.375,0.));
#14684=CARTESIAN_POINT('',(-0.35,0.35,-4.28626379701573E-17));
#14685=CARTESIAN_POINT('Origin',(0.,0.35,0.));
#14686=CARTESIAN_POINT('',(-0.325,0.375,-3.9801020972289E-17));
#14687=CARTESIAN_POINT('Origin',(0.,0.19,0.));
#14688=CARTESIAN_POINT('',(-0.35,0.03,-4.28626379701574E-17));
#14689=CARTESIAN_POINT('Origin',(0.,0.03,0.));
#14690=CARTESIAN_POINT('',(-0.35,0.19,-4.28626379701574E-17));
#14691=CARTESIAN_POINT('Origin',(0.,0.0149999999999999,0.));
#14692=CARTESIAN_POINT('',(-0.32,-3.29597460435593E-17,-3.91886975727153E-17));
#14693=CARTESIAN_POINT('Origin',(0.,0.,0.));
#14694=CARTESIAN_POINT('',(-0.335,0.0149999999999999,-4.10256677714363E-17));
#14695=CARTESIAN_POINT('Origin',(0.22,0.,0.));
#14696=CARTESIAN_POINT('',(-0.22,-6.93889390390723E-18,-2.69422295812418E-17));
#14697=CARTESIAN_POINT('Origin',(0.,0.,0.));
#14698=CARTESIAN_POINT('Origin',(0.,-0.02,0.));
#14699=CARTESIAN_POINT('',(-0.1954,-0.0492,2.39295984553393E-17));
#14700=CARTESIAN_POINT('Origin',(0.,-0.0492,0.));
#14701=CARTESIAN_POINT('',(-0.21,-0.02,-2.57175827820944E-17));
#14702=CARTESIAN_POINT('Origin',(0.,-0.8,0.));
#14703=CARTESIAN_POINT('',(-0.1954,-0.8,-2.39295984553393E-17));
#14823=UNCERTAINTY_MEASURE_WITH_UNIT(LENGTH_MEASURE(0.001),#14879,
'DISTANCE_ACCURACY_VALUE',
'Maximum model space distance between geometric entities at asserted c
onnectivities');
#14824=UNCERTAINTY_MEASURE_WITH_UNIT(LENGTH_MEASURE(0.001),#14879,
'DISTANCE_ACCURACY_VALUE',
'Maximum model space distance between geometric entities at asserted c
onnectivities');
#14877=(
GEOMETRIC_REPRESENTATION_CONTEXT(3)
GLOBAL_UNCERTAINTY_ASSIGNED_CONTEXT((#14823))
GLOBAL_UNIT_ASSIGNED_CONTEXT((#14879,#14881,#14882))
REPRESENTATION_CONTEXT('','3D')
);
#14878=(
GEOMETRIC_REPRESENTATION_CONTEXT(3)
GLOBAL_UNCERTAINTY_ASSIGNED_CONTEXT((#14824))
GLOBAL_UNIT_ASSIGNED_CONTEXT((#14879,#14881,#14882))
REPRESENTATION_CONTEXT('','3D')
);
#14879=(
LENGTH_UNIT()
NAMED_UNIT(*)
SI_UNIT(.CENTI.,.METRE.)
);
#14881=(
NAMED_UNIT(*)
PLANE_ANGLE_UNIT()
SI_UNIT($,.RADIAN.)
);
#14882=(
NAMED_UNIT(*)
SI_UNIT($,.STERADIAN.)
SOLID_ANGLE_UNIT()
);
#14935=SHAPE_DEFINITION_REPRESENTATION(#15000,#15120);
#15000=PRODUCT_DEFINITION_SHAPE('',$,#15174);
#15120=SHAPE_REPRESENTATION('',(#9306),#14877);
#15121=PRODUCT_DEFINITION_CONTEXT('part definition',#15282,'design');
#15174=PRODUCT_DEFINITION('M4x10 Cap Screw','M4x10 Cap Screw',#15227,#15121);
#15227=PRODUCT_DEFINITION_FORMATION('',$,#15336);
#15282=APPLICATION_CONTEXT(
'Core Data for Automotive Mechanical Design Process');
#15283=PRODUCT_CONTEXT('part definition',#15282,'mechanical');
#15336=PRODUCT('M4x10 Cap Screw','M4x10 Cap Screw','M4x10 Cap Screw',(#15283));
#15407=COLOUR_RGB('Black',0.12,0.14,0.17);
#15408=FILL_AREA_STYLE_COLOUR('',#15407);
#15409=FILL_AREA_STYLE('',(#15408));
#15410=SURFACE_STYLE_FILL_AREA(#15409);
#15411=SURFACE_SIDE_STYLE('',(#15410));
#15412=SURFACE_STYLE_USAGE(.BOTH.,#15411);
#15413=PRESENTATION_STYLE_ASSIGNMENT((#15412));
ENDSEC;
END-ISO-10303-21;
